ISO-10303-21;
HEADER;
/* Generated by software containing ST-Developer
 * from STEP Tools, Inc. (www.steptools.com) 
 */

FILE_DESCRIPTION(
/* description */ (''),
/* implementation_level */ '2;1');

FILE_NAME(
/* name */ 'Rod_Mount_02.step',
/* time_stamp */ '2026-10-19T02:00:06+06:00',
/* author */ (''),
/* organization */ (''),
/* preprocessor_version */ 'ST-DEVELOPER v20.2',
/* originating_system */ 'Autodesk Translation Framework v15.15.0.0',
/* authorisation */ '');

FILE_SCHEMA (('AUTOMOTIVE_DESIGN { 1 0 10303 214 3 1 1 }'));
ENDSEC;

DATA;
#10=MECHANICAL_DESIGN_GEOMETRIC_PRESENTATION_REPRESENTATION('',(#114),#4833);
#92=SHAPE_REPRESENTATION_RELATIONSHIP('SRR','None',#4883,#103);
#103=ADVANCED_BREP_SHAPE_REPRESENTATION('',(#125),#4831);
#114=STYLED_ITEM('',(#4992),#125);
#125=MANIFOLD_SOLID_BREP('Rod_Mount_02',#2696);
#161=FACE_BOUND('',#611,.T.);
#162=FACE_BOUND('',#614,.T.);
#163=FACE_BOUND('',#616,.T.);
#255=PLANE('',#3062);
#256=PLANE('',#3066);
#257=PLANE('',#3067);
#413=FACE_OUTER_BOUND('',#608,.T.);
#414=FACE_OUTER_BOUND('',#609,.T.);
#415=FACE_OUTER_BOUND('',#610,.T.);
#416=FACE_OUTER_BOUND('',#612,.T.);
#417=FACE_OUTER_BOUND('',#613,.T.);
#418=FACE_OUTER_BOUND('',#615,.T.);
#608=EDGE_LOOP('',(#2407,#2408,#2409,#2410));
#609=EDGE_LOOP('',(#2411,#2412,#2413,#2414));
#610=EDGE_LOOP('',(#2415));
#611=EDGE_LOOP('',(#2416));
#612=EDGE_LOOP('',(#2417,#2418,#2419,#2420));
#613=EDGE_LOOP('',(#2421));
#614=EDGE_LOOP('',(#2422));
#615=EDGE_LOOP('',(#2423));
#616=EDGE_LOOP('',(#2424));
#854=LINE('',#4729,#1108);
#855=LINE('',#4735,#1109);
#856=LINE('',#4742,#1110);
#1108=VECTOR('',#3793,7.);
#1109=VECTOR('',#3800,6.);
#1110=VECTOR('',#3809,11.);
#1199=CIRCLE('',#3057,7.);
#1200=CIRCLE('',#3058,7.);
#1201=CIRCLE('',#3060,6.);
#1202=CIRCLE('',#3061,6.);
#1203=CIRCLE('',#3064,11.);
#1204=CIRCLE('',#3065,11.);
#1407=VERTEX_POINT('',#4726);
#1408=VERTEX_POINT('',#4728);
#1409=VERTEX_POINT('',#4732);
#1410=VERTEX_POINT('',#4734);
#1411=VERTEX_POINT('',#4739);
#1412=VERTEX_POINT('',#4741);
#1744=EDGE_CURVE('',#1407,#1407,#1199,.T.);
#1745=EDGE_CURVE('',#1407,#1408,#854,.T.);
#1746=EDGE_CURVE('',#1408,#1408,#1200,.T.);
#1747=EDGE_CURVE('',#1409,#1409,#1201,.T.);
#1748=EDGE_CURVE('',#1409,#1410,#855,.T.);
#1749=EDGE_CURVE('',#1410,#1410,#1202,.T.);
#1750=EDGE_CURVE('',#1411,#1411,#1203,.T.);
#1751=EDGE_CURVE('',#1411,#1412,#856,.T.);
#1752=EDGE_CURVE('',#1412,#1412,#1204,.T.);
#2407=ORIENTED_EDGE('',*,*,#1744,.T.);
#2408=ORIENTED_EDGE('',*,*,#1745,.T.);
#2409=ORIENTED_EDGE('',*,*,#1746,.T.);
#2410=ORIENTED_EDGE('',*,*,#1745,.F.);
#2411=ORIENTED_EDGE('',*,*,#1747,.T.);
#2412=ORIENTED_EDGE('',*,*,#1748,.T.);
#2413=ORIENTED_EDGE('',*,*,#1749,.F.);
#2414=ORIENTED_EDGE('',*,*,#1748,.F.);
#2415=ORIENTED_EDGE('',*,*,#1744,.F.);
#2416=ORIENTED_EDGE('',*,*,#1747,.F.);
#2417=ORIENTED_EDGE('',*,*,#1750,.T.);
#2418=ORIENTED_EDGE('',*,*,#1751,.T.);
#2419=ORIENTED_EDGE('',*,*,#1752,.F.);
#2420=ORIENTED_EDGE('',*,*,#1751,.F.);
#2421=ORIENTED_EDGE('',*,*,#1750,.F.);
#2422=ORIENTED_EDGE('',*,*,#1746,.F.);
#2423=ORIENTED_EDGE('',*,*,#1752,.T.);
#2424=ORIENTED_EDGE('',*,*,#1749,.T.);
#2523=CYLINDRICAL_SURFACE('',#3056,7.);
#2524=CYLINDRICAL_SURFACE('',#3059,6.);
#2525=CYLINDRICAL_SURFACE('',#3063,11.);
#2671=ADVANCED_FACE('',(#413),#2523,.T.);
#2672=ADVANCED_FACE('',(#414),#2524,.F.);
#2673=ADVANCED_FACE('',(#415,#161),#255,.F.);
#2674=ADVANCED_FACE('',(#416),#2525,.T.);
#2675=ADVANCED_FACE('',(#417,#162),#256,.F.);
#2676=ADVANCED_FACE('',(#418,#163),#257,.T.);
#2696=CLOSED_SHELL('',(#2671,#2672,#2673,#2674,#2675,#2676));
#3055=AXIS2_PLACEMENT_3D('',#4724,#3787,#3788);
#3056=AXIS2_PLACEMENT_3D('',#4725,#3789,#3790);
#3057=AXIS2_PLACEMENT_3D('',#4727,#3791,#3792);
#3058=AXIS2_PLACEMENT_3D('',#4730,#3794,#3795);
#3059=AXIS2_PLACEMENT_3D('',#4731,#3796,#3797);
#3060=AXIS2_PLACEMENT_3D('',#4733,#3798,#3799);
#3061=AXIS2_PLACEMENT_3D('',#4736,#3801,#3802);
#3062=AXIS2_PLACEMENT_3D('',#4737,#3803,#3804);
#3063=AXIS2_PLACEMENT_3D('',#4738,#3805,#3806);
#3064=AXIS2_PLACEMENT_3D('',#4740,#3807,#3808);
#3065=AXIS2_PLACEMENT_3D('',#4743,#3810,#3811);
#3066=AXIS2_PLACEMENT_3D('',#4744,#3812,#3813);
#3067=AXIS2_PLACEMENT_3D('',#4745,#3814,#3815);
#3787=DIRECTION('axis',(0.,0.,1.));
#3788=DIRECTION('refdir',(1.,0.,0.));
#3789=DIRECTION('center_axis',(-1.,0.,0.));
#3790=DIRECTION('ref_axis',(0.,-1.,0.));
#3791=DIRECTION('center_axis',(-1.,0.,0.));
#3792=DIRECTION('ref_axis',(0.,-1.,0.));
#3793=DIRECTION('',(-1.,0.,0.));
#3794=DIRECTION('center_axis',(1.,0.,0.));
#3795=DIRECTION('ref_axis',(0.,-1.,0.));
#3796=DIRECTION('center_axis',(-1.,0.,0.));
#3797=DIRECTION('ref_axis',(0.,-1.,0.));
#3798=DIRECTION('center_axis',(1.,0.,0.));
#3799=DIRECTION('ref_axis',(0.,-1.,0.));
#3800=DIRECTION('',(-1.,0.,0.));
#3801=DIRECTION('center_axis',(1.,0.,0.));
#3802=DIRECTION('ref_axis',(0.,-1.,0.));
#3803=DIRECTION('center_axis',(-1.,0.,0.));
#3804=DIRECTION('ref_axis',(0.,-1.,0.));
#3805=DIRECTION('center_axis',(-1.,0.,0.));
#3806=DIRECTION('ref_axis',(0.,-1.,0.));
#3807=DIRECTION('center_axis',(-1.,0.,0.));
#3808=DIRECTION('ref_axis',(0.,-1.,0.));
#3809=DIRECTION('',(-1.,0.,0.));
#3810=DIRECTION('center_axis',(-1.,0.,0.));
#3811=DIRECTION('ref_axis',(0.,-1.,0.));
#3812=DIRECTION('center_axis',(-1.,0.,0.));
#3813=DIRECTION('ref_axis',(0.,-1.,0.));
#3814=DIRECTION('center_axis',(-1.,0.,0.));
#3815=DIRECTION('ref_axis',(0.,-1.,0.));
#4724=CARTESIAN_POINT('',(0.,0.,0.));
#4725=CARTESIAN_POINT('Origin',(-90.,-30.0000000000105,7.00000000000211));
#4726=CARTESIAN_POINT('',(-80.,-23.0000000000105,7.00000000000211));
#4727=CARTESIAN_POINT('Origin',(-80.,-30.0000000000105,7.00000000000211));
#4728=CARTESIAN_POINT('',(-89.,-23.0000000000105,7.00000000000211));
#4729=CARTESIAN_POINT('',(-90.,-23.0000000000105,7.00000000000211));
#4730=CARTESIAN_POINT('Origin',(-89.,-30.0000000000105,7.00000000000211));
#4731=CARTESIAN_POINT('Origin',(-90.,-30.0000000000105,7.00000000000211));
#4732=CARTESIAN_POINT('',(-80.,-24.0000000000105,7.00000000000211));
#4733=CARTESIAN_POINT('Origin',(-80.,-30.0000000000105,7.00000000000211));
#4734=CARTESIAN_POINT('',(-90.,-24.0000000000105,7.00000000000211));
#4735=CARTESIAN_POINT('',(-90.,-24.0000000000105,7.00000000000211));
#4736=CARTESIAN_POINT('Origin',(-90.,-30.0000000000105,7.00000000000211));
#4737=CARTESIAN_POINT('Origin',(-80.,-30.0000000000105,7.00000000000211));
#4738=CARTESIAN_POINT('Origin',(-90.,-30.0000000000105,7.00000000000211));
#4739=CARTESIAN_POINT('',(-89.,-19.0000000000105,7.00000000000211));
#4740=CARTESIAN_POINT('Origin',(-89.,-30.0000000000105,7.00000000000211));
#4741=CARTESIAN_POINT('',(-90.,-19.0000000000105,7.00000000000211));
#4742=CARTESIAN_POINT('',(-90.,-19.0000000000105,7.00000000000211));
#4743=CARTESIAN_POINT('Origin',(-90.,-30.0000000000105,7.00000000000211));
#4744=CARTESIAN_POINT('Origin',(-89.,-30.0000000000105,7.00000000000211));
#4745=CARTESIAN_POINT('Origin',(-90.,-30.0000000000105,7.00000000000211));
#4818=UNCERTAINTY_MEASURE_WITH_UNIT(LENGTH_MEASURE(0.01),#4834,
'DISTANCE_ACCURACY_VALUE',
'Maximum model space distance between geometric entities at asserted c
onnectivities');
#4820=UNCERTAINTY_MEASURE_WITH_UNIT(LENGTH_MEASURE(0.01),#4834,
'DISTANCE_ACCURACY_VALUE',
'Maximum model space distance between geometric entities at asserted c
onnectivities');
#4831=(
GEOMETRIC_REPRESENTATION_CONTEXT(3)
GLOBAL_UNCERTAINTY_ASSIGNED_CONTEXT((#4818))
GLOBAL_UNIT_ASSIGNED_CONTEXT((#4834,#4836,#4837))
REPRESENTATION_CONTEXT('','3D')
);
#4833=(
GEOMETRIC_REPRESENTATION_CONTEXT(3)
GLOBAL_UNCERTAINTY_ASSIGNED_CONTEXT((#4820))
GLOBAL_UNIT_ASSIGNED_CONTEXT((#4834,#4836,#4837))
REPRESENTATION_CONTEXT('','3D')
);
#4834=(
LENGTH_UNIT()
NAMED_UNIT(*)
SI_UNIT(.MILLI.,.METRE.)
);
#4836=(
NAMED_UNIT(*)
PLANE_ANGLE_UNIT()
SI_UNIT($,.RADIAN.)
);
#4837=(
NAMED_UNIT(*)
SI_UNIT($,.STERADIAN.)
SOLID_ANGLE_UNIT()
);
#4848=SHAPE_DEFINITION_REPRESENTATION(#4860,#4883);
#4860=PRODUCT_DEFINITION_SHAPE('',$,#4896);
#4883=SHAPE_REPRESENTATION('',(#3055),#4831);
#4885=PRODUCT_DEFINITION_CONTEXT('part definition',#4923,'design');
#4896=PRODUCT_DEFINITION('Rod_Mount_02','Rod_Mount_02',#4908,#4885);
#4908=PRODUCT_DEFINITION_FORMATION('',$,#4935);
#4923=APPLICATION_CONTEXT(
'Core Data for Automotive Mechanical Design Process');
#4924=PRODUCT_CONTEXT('part definition',#4923,'mechanical');
#4935=PRODUCT('Rod_Mount_02','Rod_Mount_02',$,(#4924));
#4986=COLOUR_RGB('Grey',0.48,0.52,0.57);
#4987=FILL_AREA_STYLE_COLOUR('',#4986);
#4988=FILL_AREA_STYLE('',(#4987));
#4989=SURFACE_STYLE_FILL_AREA(#4988);
#4990=SURFACE_SIDE_STYLE('',(#4989));
#4991=SURFACE_STYLE_USAGE(.BOTH.,#4990);
#4992=PRESENTATION_STYLE_ASSIGNMENT((#4991));
ENDSEC;
END-ISO-10303-21;
